ISO-10303-21;
HEADER;
FILE_DESCRIPTION (('STEP AP214'),
    '1' );
FILE_NAME ('Part1.step',
    '2026-10-09T16:01:55',
    ( '' ),
    ( '' ),
    'SwSTEP 2.0',
    'SolidWorks 2024',
    '' );
FILE_SCHEMA (( 'AUTOMOTIVE_DESIGN' ));
ENDSEC;

DATA;
#75=ORIENTED_EDGE ( 'NONE', *, *, #18728, .F. ) ;
#382=FACE_OUTER_BOUND ( 'NONE', #42466, .T. ) ;
#527=VERTEX_POINT ( 'NONE', #49303 ) ;
#720=AXIS2_PLACEMENT_3D ( 'NONE', #47472, #10687, #69040 ) ;
#815=EDGE_CURVE ( 'NONE', #68276, #10103, #58910, .T. ) ;
#1045=DIRECTION ( 'NONE',  ( -0.000000000000000000, 1.000000000000000000, -0.000000000000000000 ) ) ;
#1062=DIRECTION ( 'NONE',  ( -0.000000000000000000, 1.000000000000000000, -0.000000000000000000 ) ) ;
#1126=DIRECTION ( 'NONE',  ( -0.000000000000000000, 1.000000000000000000, -0.000000000000000000 ) ) ;
#1153=AXIS2_PLACEMENT_3D ( 'NONE', #46137, #13612, #29873 ) ;
#1260=DIRECTION ( 'NONE',  ( -0.000000000000000000, -1.000000000000000000, -0.000000000000000000 ) ) ;
#1715=CARTESIAN_POINT ( 'NONE',  ( 75.42576880091934299, 0.000000000000000000, 327.4830310981788557 ) ) ;
#1891=AXIS2_PLACEMENT_3D ( 'NONE', #9973, #30120, #31539 ) ;
#1972=CARTESIAN_POINT ( 'NONE',  ( 106.4257688009193430, 10.00000000000000000, 334.4830310981789694 ) ) ;
#2328=ADVANCED_FACE ( 'NONE', ( #56254 ), #29031, .F. ) ;
#2634=EDGE_CURVE ( 'NONE', #19716, #24845, #7714, .T. ) ;
#3077=DIRECTION ( 'NONE',  ( -1.000000000000000000, 0.000000000000000000, -8.480870326997715333E-15 ) ) ;
#3287=LINE ( 'NONE', #40045, #20947 ) ;
#3369=CARTESIAN_POINT ( 'NONE',  ( 106.4257688009193998, 10.00000000000000000, 285.9830310981789125 ) ) ;
#3504=FACE_OUTER_BOUND ( 'NONE', #69071, .T. ) ;
#3801=ORIENTED_EDGE ( 'NONE', *, *, #39425, .F. ) ;
#3941=CYLINDRICAL_SURFACE ( 'NONE', #30567, 3.500000000000003109 ) ;
#4022=ORIENTED_EDGE ( 'NONE', *, *, #36112, .F. ) ;
#4051=CIRCLE ( 'NONE', #39059, 3.500000000000003109 ) ;
#4123=DIRECTION ( 'NONE',  ( 0.000000000000000000, 1.000000000000000000, 0.000000000000000000 ) ) ;
#4306=FACE_OUTER_BOUND ( 'NONE', #37137, .T. ) ;
#4333=EDGE_CURVE ( 'NONE', #10103, #68276, #26662, .T. ) ;
#4341=( GEOMETRIC_REPRESENTATION_CONTEXT ( 3 ) GLOBAL_UNCERTAINTY_ASSIGNED_CONTEXT ( ( #9763 ) ) GLOBAL_UNIT_ASSIGNED_CONTEXT ( ( #4671, #19867, #35783 ) ) REPRESENTATION_CONTEXT ( 'NONE', 'WORKASPACE' ) );
#4483=DIRECTION ( 'NONE',  ( 0.000000000000000000, 0.000000000000000000, 1.000000000000000000 ) ) ;
#4641=CARTESIAN_POINT ( 'NONE',  ( 106.4257688009193998, 0.000000000000000000, 285.9830310981789125 ) ) ;
#4657=DIRECTION ( 'NONE',  ( 1.000000000000000000, 0.000000000000000000, 0.000000000000000000 ) ) ;
#4665=ORIENTED_EDGE ( 'NONE', *, *, #30439, .F. ) ;
#4671=( LENGTH_UNIT ( ) NAMED_UNIT ( * ) SI_UNIT ( .MILLI., .METRE. ) );
#4687=ORIENTED_EDGE ( 'NONE', *, *, #34281, .T. ) ;
#4831=DIRECTION ( 'NONE',  ( -0.000000000000000000, 1.000000000000000000, -0.000000000000000000 ) ) ;
#4917=CARTESIAN_POINT ( 'NONE',  ( 106.4257688009193430, 0.000000000000000000, 330.9830310981789694 ) ) ;
#5000=DIRECTION ( 'NONE',  ( 0.000000000000000000, 0.000000000000000000, 1.000000000000000000 ) ) ;
#5039=CARTESIAN_POINT ( 'NONE',  ( 69.92576880110368620, 10.00000000000000000, 281.4830310981151911 ) ) ;
#5114=AXIS2_PLACEMENT_3D ( 'NONE', #42049, #31805, #26149 ) ;
#5134=ORIENTED_EDGE ( 'NONE', *, *, #53278, .T. ) ;
#5182=CARTESIAN_POINT ( 'NONE',  ( 75.42576880091937142, 0.000000000000000000, 285.9830310981789125 ) ) ;
#5871=DIRECTION ( 'NONE',  ( 0.000000000000000000, 1.000000000000000000, 0.000000000000000000 ) ) ;
#6371=PLANE ( 'NONE',  #16998 ) ;
#6699=DIRECTION ( 'NONE',  ( 0.000000000000000000, 1.000000000000000000, 0.000000000000000000 ) ) ;
#6757=FACE_OUTER_BOUND ( 'NONE', #44291, .T. ) ;
#6803=EDGE_CURVE ( 'NONE', #27638, #35258, #50931, .T. ) ;
#7034=DIRECTION ( 'NONE',  ( 0.000000000000000000, 0.000000000000000000, 1.000000000000000000 ) ) ;
#7101=CARTESIAN_POINT ( 'NONE',  ( 69.92576880110416937, 10.00000000000000000, 335.4830310981152479 ) ) ;
#7422=DIRECTION ( 'NONE',  ( 8.994862468027880808E-15, 0.000000000000000000, 1.000000000000000000 ) ) ;
#7423=CARTESIAN_POINT ( 'NONE',  ( 111.9257688011037146, 0.000000000000000000, 335.4830310981152479 ) ) ;
#7469=CARTESIAN_POINT ( 'NONE',  ( 75.42576880091934299, 0.000000000000000000, 334.4830310981790831 ) ) ;
#7662=PLANE ( 'NONE',  #42257 ) ;
#7714=LINE ( 'NONE', #66071, #54562 ) ;
#8117=ADVANCED_BREP_SHAPE_REPRESENTATION ( '', ( #21303, #45918 ), #66261 ) ;
#8551=EDGE_LOOP ( 'NONE', ( #66177, #48081 ) ) ;
#8744=CARTESIAN_POINT ( 'NONE',  ( 75.42576880091937142, 0.000000000000000000, 285.9830310981789125 ) ) ;
#8841=DIRECTION ( 'NONE',  ( -8.994862468027880808E-15, 0.000000000000000000, -1.000000000000000000 ) ) ;
#9081=DIRECTION ( 'NONE',  ( -0.000000000000000000, 1.000000000000000000, -0.000000000000000000 ) ) ;
#9227=VECTOR ( 'NONE', #32896, 1000.000000000000000 ) ;
#9264=CARTESIAN_POINT ( 'NONE',  ( 69.92576880110368620, 10.00000000000000000, 281.4830310981151911 ) ) ;
#9409=ORIENTED_EDGE ( 'NONE', *, *, #15667, .T. ) ;
#9426=FACE_OUTER_BOUND ( 'NONE', #69733, .T. ) ;
#9530=VERTEX_POINT ( 'NONE', #18970 ) ;
#9540=EDGE_CURVE ( 'NONE', #23385, #20190, #28865, .T. ) ;
#9597=DIRECTION ( 'NONE',  ( -0.000000000000000000, 1.000000000000000000, -0.000000000000000000 ) ) ;
#9763=UNCERTAINTY_MEASURE_WITH_UNIT (LENGTH_MEASURE( 1.000000000000000082E-05 ), #4671, 'distance_accuracy_value', 'NONE');
#9973=CARTESIAN_POINT ( 'NONE',  ( 0.000000000000000000, 10.00000000000000000, 0.000000000000000000 ) ) ;
#10091=ADVANCED_FACE ( 'NONE', ( #382 ), #59432, .F. ) ;
#10103=VERTEX_POINT ( 'NONE', #15254 ) ;
#10133=CARTESIAN_POINT ( 'NONE',  ( 106.4257688009193430, 0.000000000000000000, 334.4830310981789694 ) ) ;
#10298=DIRECTION ( 'NONE',  ( 0.000000000000000000, 1.000000000000000000, 0.000000000000000000 ) ) ;
#10349=PLANE ( 'NONE',  #67077 ) ;
#10431=ORIENTED_EDGE ( 'NONE', *, *, #40306, .T. ) ;
#10444=ORIENTED_EDGE ( 'NONE', *, *, #64810, .F. ) ;
#10641=EDGE_CURVE ( 'NONE', #9530, #27811, #38801, .T. ) ;
#10687=DIRECTION ( 'NONE',  ( 0.000000000000000000, 1.000000000000000000, 0.000000000000000000 ) ) ;
#10777=ADVANCED_FACE ( 'NONE', ( #67431 ), #7662, .F. ) ;
#11278=ORIENTED_EDGE ( 'NONE', *, *, #30439, .T. ) ;
#11319=LINE ( 'NONE', #16983, #9227 ) ;
#11340=LINE ( 'NONE', #37885, #49914 ) ;
#11535=EDGE_LOOP ( 'NONE', ( #35950, #41358, #53049, #25058 ) ) ;
#12334=DIRECTION ( 'NONE',  ( 0.000000000000000000, -0.000000000000000000, 1.000000000000000000 ) ) ;
#12660=DIRECTION ( 'NONE',  ( -0.000000000000000000, -1.000000000000000000, -0.000000000000000000 ) ) ;
#12825=DIRECTION ( 'NONE',  ( -0.000000000000000000, 1.000000000000000000, -0.000000000000000000 ) ) ;
#12843=ORIENTED_EDGE ( 'NONE', *, *, #67554, .F. ) ;
#13119=ORIENTED_EDGE ( 'NONE', *, *, #69564, .T. ) ;
#13154=CARTESIAN_POINT ( 'NONE',  ( 69.92576880110368620, 0.000000000000000000, 281.4830310981151911 ) ) ;
#13212=VECTOR ( 'NONE', #1045, 1000.000000000000000 ) ;
#13390=FACE_OUTER_BOUND ( 'NONE', #13486, .T. ) ;
#13486=EDGE_LOOP ( 'NONE', ( #20968, #47499, #60611, #67740 ) ) ;
#13565=ORIENTED_EDGE ( 'NONE', *, *, #14865, .F. ) ;
#13612=DIRECTION ( 'NONE',  ( 0.000000000000000000, 1.000000000000000000, 0.000000000000000000 ) ) ;
#13728=EDGE_CURVE ( 'NONE', #20190, #24845, #66815, .T. ) ;
#13949=ORIENTED_EDGE ( 'NONE', *, *, #15667, .F. ) ;
#14025=DIRECTION ( 'NONE',  ( 0.000000000000000000, 1.000000000000000000, 0.000000000000000000 ) ) ;
#14038=CYLINDRICAL_SURFACE ( 'NONE', #29955, 3.500000000000003109 ) ;
#14263=ADVANCED_FACE ( 'NONE', ( #30663 ), #14038, .F. ) ;
#14425=ORIENTED_EDGE ( 'NONE', *, *, #45326, .T. ) ;
#14729=VECTOR ( 'NONE', #1260, 1000.000000000000000 ) ;
#14783=DIRECTION ( 'NONE',  ( -0.000000000000000000, 1.000000000000000000, -0.000000000000000000 ) ) ;
#14856=PLANE ( 'NONE',  #40412 ) ;
#14863=ORIENTED_EDGE ( 'NONE', *, *, #55375, .T. ) ;
#14865=EDGE_CURVE ( 'NONE', #62405, #22621, #41542, .T. ) ;
#14944=DIRECTION ( 'NONE',  ( 0.000000000000000000, 0.000000000000000000, 1.000000000000000000 ) ) ;
#14954=DIRECTION ( 'NONE',  ( 1.000000000000000000, 0.000000000000000000, -0.000000000000000000 ) ) ;
#15135=CARTESIAN_POINT ( 'NONE',  ( 75.42576880091937142, 0.000000000000000000, 289.4830310981789125 ) ) ;
#15254=CARTESIAN_POINT ( 'NONE',  ( 75.42576880091934299, 10.00000000000000000, 327.4830310981788557 ) ) ;
#15258=CARTESIAN_POINT ( 'NONE',  ( 106.4257688009193430, 10.00000000000000000, 330.9830310981789694 ) ) ;
#15402=ORIENTED_EDGE ( 'NONE', *, *, #815, .F. ) ;
#15667=EDGE_CURVE ( 'NONE', #48443, #9530, #22252, .T. ) ;
#15852=EDGE_CURVE ( 'NONE', #42826, #57404, #48247, .T. ) ;
#15940=EDGE_LOOP ( 'NONE', ( #13119, #13565, #3801, #33955 ) ) ;
#16114=DIRECTION ( 'NONE',  ( 0.000000000000000000, 0.000000000000000000, 1.000000000000000000 ) ) ;
#16164=CIRCLE ( 'NONE', #42151, 3.500000000000003109 ) ;
#16213=DIRECTION ( 'NONE',  ( 0.000000000000000000, 0.000000000000000000, 1.000000000000000000 ) ) ;
#16411=CARTESIAN_POINT ( 'NONE',  ( 75.42576880091934299, 0.000000000000000000, 330.9830310981789694 ) ) ;
#16419=CARTESIAN_POINT ( 'NONE',  ( 75.42576880091937142, 10.00000000000000000, 282.4830310981789125 ) ) ;
#16483=LINE ( 'NONE', #55018, #14729 ) ;
#16983=CARTESIAN_POINT ( 'NONE',  ( 69.92576880110368620, 10.00000000000000000, 281.4830310981151911 ) ) ;
#16998=AXIS2_PLACEMENT_3D ( 'NONE', #60789, #6699, #12334 ) ;
#17002=ORIENTED_EDGE ( 'NONE', *, *, #40431, .T. ) ;
#17025=ORIENTED_EDGE ( 'NONE', *, *, #15852, .T. ) ;
#17027=ORIENTED_EDGE ( 'NONE', *, *, #43630, .T. ) ;
#17086=ORIENTED_EDGE ( 'NONE', *, *, #36112, .T. ) ;
#17120=PRODUCT_DEFINITION ( 'UNKNOWN', '', #35823, #40234 ) ;
#17748=AXIS2_PLACEMENT_3D ( 'NONE', #19330, #14025, #47609 ) ;
#17819=APPLICATION_CONTEXT ( 'automotive_design' ) ;
#18064=DIRECTION ( 'NONE',  ( -1.000000000000000000, 0.000000000000000000, -0.000000000000000000 ) ) ;
#18157=( LENGTH_UNIT ( ) NAMED_UNIT ( * ) SI_UNIT ( .MILLI., .METRE. ) );
#18277=PRODUCT_DEFINITION_SHAPE ( 'NONE', 'NONE',  #17120 ) ;
#18602=DIRECTION ( 'NONE',  ( 0.000000000000000000, 1.000000000000000000, 0.000000000000000000 ) ) ;
#18655=VERTEX_POINT ( 'NONE', #1972 ) ;
#18657=CIRCLE ( 'NONE', #5114, 3.500000000000003109 ) ;
#18728=EDGE_CURVE ( 'NONE', #57404, #42826, #66198, .T. ) ;
#18970=CARTESIAN_POINT ( 'NONE',  ( 106.4257688009193430, 0.000000000000000000, 327.4830310981789694 ) ) ;
#19181=CARTESIAN_POINT ( 'NONE',  ( 69.92576880110368620, 10.00000000000000000, 281.4830310981151911 ) ) ;
#19267=DIRECTION ( 'NONE',  ( -1.000000000000000000, -0.000000000000000000, -0.000000000000000000 ) ) ;
#19330=CARTESIAN_POINT ( 'NONE',  ( 106.4257688009193998, 10.00000000000000000, 285.9830310981789125 ) ) ;
#19622=ORIENTED_EDGE ( 'NONE', *, *, #42789, .T. ) ;
#19716=VERTEX_POINT ( 'NONE', #43329 ) ;
#19856=FACE_BOUND ( 'NONE', #34695, .T. ) ;
#19866=VECTOR ( 'NONE', #64512, 1000.000000000000000 ) ;
#19867=( NAMED_UNIT ( * ) PLANE_ANGLE_UNIT ( ) SI_UNIT ( $, .RADIAN. ) );
#20175=ORIENTED_EDGE ( 'NONE', *, *, #815, .T. ) ;
#20190=VERTEX_POINT ( 'NONE', #13154 ) ;
#20239=DIRECTION ( 'NONE',  ( 0.000000000000000000, 1.000000000000000000, 0.000000000000000000 ) ) ;
#20323=ADVANCED_FACE ( 'NONE', ( #25881, #19856, #41429, #36846, #58415 ), #47782, .T. ) ;
#20385=DIRECTION ( 'NONE',  ( -0.000000000000000000, 1.000000000000000000, -0.000000000000000000 ) ) ;
#20565=DIRECTION ( 'NONE',  ( -1.000000000000000000, -0.000000000000000000, -0.000000000000000000 ) ) ;
#20765=ORIENTED_EDGE ( 'NONE', *, *, #40216, .T. ) ;
#20947=VECTOR ( 'NONE', #12825, 1000.000000000000000 ) ;
#20968=ORIENTED_EDGE ( 'NONE', *, *, #40216, .F. ) ;
#21242=COLOUR_RGB ( '', 0.31764706, 0.68627451, 0.89019608) ;
#21303=MANIFOLD_SOLID_BREP ( 'Cut-Extrude3', #43096 ) ;
#21494=AXIS2_PLACEMENT_3D ( 'NONE', #5182, #36299, #42299 ) ;
#21935=EDGE_CURVE ( 'NONE', #35258, #42826, #51885, .T. ) ;
#22042=ORIENTED_EDGE ( 'NONE', *, *, #69213, .T. ) ;
#22252=CIRCLE ( 'NONE', #31306, 3.500000000000003109 ) ;
#22340=ORIENTED_EDGE ( 'NONE', *, *, #10641, .T. ) ;
#22536=DIRECTION ( 'NONE',  ( 0.000000000000000000, 0.000000000000000000, 1.000000000000000000 ) ) ;
#22621=VERTEX_POINT ( 'NONE', #7423 ) ;
#22651=VECTOR ( 'NONE', #19267, 1000.000000000000000 ) ;
#22685=CARTESIAN_POINT ( 'NONE',  ( 106.4257688009193998, 0.000000000000000000, 285.9830310981789125 ) ) ;
#22775=CARTESIAN_POINT ( 'NONE',  ( 0.000000000000000000, 0.000000000000000000, 0.000000000000000000 ) ) ;
#22937=CARTESIAN_POINT ( 'NONE',  ( 75.42576880091934299, 0.000000000000000000, 327.4830310981788557 ) ) ;
#23268=CIRCLE ( 'NONE', #65082, 3.500000000000003109 ) ;
#23305=ADVANCED_FACE ( 'NONE', ( #28735 ), #34035, .F. ) ;
#23317=AXIS2_PLACEMENT_3D ( 'NONE', #15258, #10298, #30812 ) ;
#23385=VERTEX_POINT ( 'NONE', #19181 ) ;
#23752=EDGE_LOOP ( 'NONE', ( #75, #26966 ) ) ;
#23916=ADVANCED_FACE ( 'NONE', ( #62568 ), #14856, .F. ) ;
#24169=EDGE_LOOP ( 'NONE', ( #19622, #31925, #64043, #14863 ) ) ;
#24547=DIRECTION ( 'NONE',  ( 0.000000000000000000, 1.000000000000000000, 0.000000000000000000 ) ) ;
#24845=VERTEX_POINT ( 'NONE', #57721 ) ;
#25058=ORIENTED_EDGE ( 'NONE', *, *, #14865, .T. ) ;
#25425=CARTESIAN_POINT ( 'NONE',  ( 75.42576880091934299, 0.000000000000000000, 334.4830310981790831 ) ) ;
#25653=DIRECTION ( 'NONE',  ( 0.000000000000000000, 1.000000000000000000, 0.000000000000000000 ) ) ;
#25863=DIRECTION ( 'NONE',  ( -0.000000000000000000, 1.000000000000000000, -0.000000000000000000 ) ) ;
#25881=FACE_BOUND ( 'NONE', #8551, .T. ) ;
#26149=DIRECTION ( 'NONE',  ( 0.000000000000000000, 0.000000000000000000, 1.000000000000000000 ) ) ;
#26204=DIRECTION ( 'NONE',  ( 0.000000000000000000, 0.000000000000000000, 1.000000000000000000 ) ) ;
#26209=VECTOR ( 'NONE', #20565, 1000.000000000000000 ) ;
#26210=CARTESIAN_POINT ( 'NONE',  ( 75.42576880091934299, 0.000000000000000000, 330.9830310981789694 ) ) ;
#26476=DIRECTION ( 'NONE',  ( -0.000000000000000000, 1.000000000000000000, -0.000000000000000000 ) ) ;
#26626=AXIS2_PLACEMENT_3D ( 'NONE', #69000, #27602, #5000 ) ;
#26662=CIRCLE ( 'NONE', #720, 3.500000000000114131 ) ;
#26723=PRODUCT ( 'Part1', 'Part1', '', ( #57566 ) ) ;
#26966=ORIENTED_EDGE ( 'NONE', *, *, #15852, .F. ) ;
#27232=ORIENTED_EDGE ( 'NONE', *, *, #69213, .F. ) ;
#27602=DIRECTION ( 'NONE',  ( 0.000000000000000000, 1.000000000000000000, 0.000000000000000000 ) ) ;
#27638=VERTEX_POINT ( 'NONE', #32889 ) ;
#27811=VERTEX_POINT ( 'NONE', #65421 ) ;
#27843=ADVANCED_FACE ( 'NONE', ( #66783, #54807, #66091, #50537, #33577 ), #6371, .F. ) ;
#28301=CARTESIAN_POINT ( 'NONE',  ( 69.92576880110368620, 0.000000000000000000, 281.4830310981151911 ) ) ;
#28470=CIRCLE ( 'NONE', #60084, 3.500000000000003109 ) ;
#28611=AXIS2_PLACEMENT_3D ( 'NONE', #45934, #35660, #67514 ) ;
#28679=DIRECTION ( 'NONE',  ( 0.000000000000000000, 0.000000000000000000, -1.000000000000000000 ) ) ;
#28735=FACE_OUTER_BOUND ( 'NONE', #45960, .T. ) ;
#28862=CIRCLE ( 'NONE', #26626, 3.500000000000114131 ) ;
#28865=LINE ( 'NONE', #45124, #41690 ) ;
#29031=PLANE ( 'NONE',  #44286 ) ;
#29139=CARTESIAN_POINT ( 'NONE',  ( 106.4257688009193430, 0.000000000000000000, 330.9830310981789694 ) ) ;
#29289=VECTOR ( 'NONE', #4657, 1000.000000000000000 ) ;
#29399=VECTOR ( 'NONE', #4831, 1000.000000000000000 ) ;
#29873=DIRECTION ( 'NONE',  ( 0.000000000000000000, 0.000000000000000000, 1.000000000000000000 ) ) ;
#29955=AXIS2_PLACEMENT_3D ( 'NONE', #8744, #30315, #45511 ) ;
#29959=CARTESIAN_POINT ( 'NONE',  ( 106.4257688009193998, 10.00000000000000000, 289.4830310981789125 ) ) ;
#30120=DIRECTION ( 'NONE',  ( 0.000000000000000000, 1.000000000000000000, 0.000000000000000000 ) ) ;
#30262=MECHANICAL_DESIGN_GEOMETRIC_PRESENTATION_REPRESENTATION('',(#48337),#4341);
#30315=DIRECTION ( 'NONE',  ( -0.000000000000000000, 1.000000000000000000, -0.000000000000000000 ) ) ;
#30351=SHAPE_DEFINITION_REPRESENTATION ( #18277, #49776 ) ;
#30439=EDGE_CURVE ( 'NONE', #35258, #27638, #28470, .T. ) ;
#30567=AXIS2_PLACEMENT_3D ( 'NONE', #4641, #25863, #26204 ) ;
#30642=CARTESIAN_POINT ( 'NONE',  ( 111.9257688011041836, 0.000000000000000000, 281.4830310981151911 ) ) ;
#30663=FACE_OUTER_BOUND ( 'NONE', #37767, .T. ) ;
#30812=DIRECTION ( 'NONE',  ( 0.000000000000000000, 0.000000000000000000, 1.000000000000000000 ) ) ;
#30865=ORIENTED_EDGE ( 'NONE', *, *, #21935, .F. ) ;
#30995=CYLINDRICAL_SURFACE ( 'NONE', #50066, 3.500000000000003109 ) ;
#31017=VERTEX_POINT ( 'NONE', #33444 ) ;
#31043=LINE ( 'NONE', #15135, #53079 ) ;
#31108=ORIENTED_EDGE ( 'NONE', *, *, #10641, .F. ) ;
#31306=AXIS2_PLACEMENT_3D ( 'NONE', #4917, #53704, #16213 ) ;
#31429=ORIENTED_EDGE ( 'NONE', *, *, #43630, .F. ) ;
#31539=DIRECTION ( 'NONE',  ( 0.000000000000000000, -0.000000000000000000, 1.000000000000000000 ) ) ;
#31654=CIRCLE ( 'NONE', #1153, 3.500000000000003109 ) ;
#31748=VECTOR ( 'NONE', #33834, 1000.000000000000000 ) ;
#31805=DIRECTION ( 'NONE',  ( 0.000000000000000000, 1.000000000000000000, 0.000000000000000000 ) ) ;
#31925=ORIENTED_EDGE ( 'NONE', *, *, #39425, .T. ) ;
#32086=LINE ( 'NONE', #53660, #55079 ) ;
#32323=ORIENTED_EDGE ( 'NONE', *, *, #41694, .F. ) ;
#32355=DIRECTION ( 'NONE',  ( 1.000000000000000000, 0.000000000000000000, 0.000000000000000000 ) ) ;
#32477=VECTOR ( 'NONE', #26476, 1000.000000000000000 ) ;
#32542=EDGE_LOOP ( 'NONE', ( #32608, #20765 ) ) ;
#32608=ORIENTED_EDGE ( 'NONE', *, *, #41694, .T. ) ;
#32889=CARTESIAN_POINT ( 'NONE',  ( 106.4257688009193998, 0.000000000000000000, 289.4830310981789125 ) ) ;
#32896=DIRECTION ( 'NONE',  ( 8.994862468027880808E-15, 0.000000000000000000, 1.000000000000000000 ) ) ;
#33102=VERTEX_POINT ( 'NONE', #55210 ) ;
#33132=CARTESIAN_POINT ( 'NONE',  ( 106.4257688009193998, 0.000000000000000000, 285.9830310981789125 ) ) ;
#33198=ORIENTED_EDGE ( 'NONE', *, *, #52974, .T. ) ;
#33395=EDGE_LOOP ( 'NONE', ( #4022, #10444 ) ) ;
#33444=CARTESIAN_POINT ( 'NONE',  ( 75.42576880091937142, 0.000000000000000000, 282.4830310981789125 ) ) ;
#33483=DIRECTION ( 'NONE',  ( 0.000000000000000000, 1.000000000000000000, 0.000000000000000000 ) ) ;
#33502=ORIENTED_EDGE ( 'NONE', *, *, #45326, .F. ) ;
#33577=FACE_OUTER_BOUND ( 'NONE', #49425, .T. ) ;
#33597=VERTEX_POINT ( 'NONE', #1715 ) ;
#33834=DIRECTION ( 'NONE',  ( -0.000000000000000000, 1.000000000000000000, -0.000000000000000000 ) ) ;
#33955=ORIENTED_EDGE ( 'NONE', *, *, #2634, .T. ) ;
#34035=CYLINDRICAL_SURFACE ( 'NONE', #36961, 3.500000000000114131 ) ;
#34281=EDGE_CURVE ( 'NONE', #27811, #18655, #18657, .T. ) ;
#34626=DIRECTION ( 'NONE',  ( 8.480870326997715333E-15, -0.000000000000000000, -1.000000000000000000 ) ) ;
#34695=EDGE_LOOP ( 'NONE', ( #15402, #56376 ) ) ;
#34858=DIRECTION ( 'NONE',  ( 0.000000000000000000, 0.000000000000000000, 1.000000000000000000 ) ) ;
#34998=ORIENTED_EDGE ( 'NONE', *, *, #21935, .T. ) ;
#35108=( NAMED_UNIT ( * ) SI_UNIT ( $, .STERADIAN. ) SOLID_ANGLE_UNIT ( ) );
#35258=VERTEX_POINT ( 'NONE', #69693 ) ;
#35533=CIRCLE ( 'NONE', #44562, 3.500000000000114131 ) ;
#35660=DIRECTION ( 'NONE',  ( -0.000000000000000000, 1.000000000000000000, -0.000000000000000000 ) ) ;
#35716=VECTOR ( 'NONE', #7422, 1000.000000000000000 ) ;
#35783=( NAMED_UNIT ( * ) SI_UNIT ( $, .STERADIAN. ) SOLID_ANGLE_UNIT ( ) );
#35823=PRODUCT_DEFINITION_FORMATION_WITH_SPECIFIED_SOURCE ( 'ANY', '', #26723, .NOT_KNOWN. ) ;
#35950=ORIENTED_EDGE ( 'NONE', *, *, #55497, .T. ) ;
#36033=CARTESIAN_POINT ( 'NONE',  ( 111.9257688011041836, 10.00000000000000000, 281.4830310981151911 ) ) ;
#36112=EDGE_CURVE ( 'NONE', #33102, #66383, #4051, .T. ) ;
#36130=SURFACE_SIDE_STYLE ('',( #41786 ) ) ;
#36299=DIRECTION ( 'NONE',  ( 0.000000000000000000, 1.000000000000000000, 0.000000000000000000 ) ) ;
#36484=FILL_AREA_STYLE ('',( #48152 ) ) ;
#36739=LINE ( 'NONE', #25425, #32477 ) ;
#36780=DIRECTION ( 'NONE',  ( 1.000000000000000000, 0.000000000000000000, -8.994862468027880808E-15 ) ) ;
#36846=FACE_BOUND ( 'NONE', #23752, .T. ) ;
#36900=AXIS2_PLACEMENT_3D ( 'NONE', #3369, #25653, #46495 ) ;
#36961=AXIS2_PLACEMENT_3D ( 'NONE', #16411, #50310, #54947 ) ;
#37137=EDGE_LOOP ( 'NONE', ( #30865, #62833, #66439, #52019 ) ) ;
#37219=EDGE_LOOP ( 'NONE', ( #17027, #33198 ) ) ;
#37259=VECTOR ( 'NONE', #34626, 1000.000000000000000 ) ;
#37292=CARTESIAN_POINT ( 'NONE',  ( 111.9257688011037146, 10.00000000000000000, 335.4830310981152479 ) ) ;
#37767=EDGE_LOOP ( 'NONE', ( #40593, #32323, #5134, #17086 ) ) ;
#37827=VECTOR ( 'NONE', #9081, 1000.000000000000000 ) ;
#37885=CARTESIAN_POINT ( 'NONE',  ( 111.9257688011041836, 0.000000000000000000, 281.4830310981151911 ) ) ;
#38143=ORIENTED_EDGE ( 'NONE', *, *, #52974, .F. ) ;
#38172=AXIS2_PLACEMENT_3D ( 'NONE', #26210, #9597, #52751 ) ;
#38180=APPLICATION_CONTEXT ( 'automotive_design' ) ;
#38630=ORIENTED_EDGE ( 'NONE', *, *, #40306, .F. ) ;
#38801=LINE ( 'NONE', #54735, #31748 ) ;
#39059=AXIS2_PLACEMENT_3D ( 'NONE', #63517, #4123, #16114 ) ;
#39187=ORIENTED_EDGE ( 'NONE', *, *, #2634, .F. ) ;
#39202=LINE ( 'NONE', #22937, #13212 ) ;
#39425=EDGE_CURVE ( 'NONE', #19716, #62405, #64742, .T. ) ;
#39745=EDGE_CURVE ( 'NONE', #62405, #527, #62913, .T. ) ;
#40045=CARTESIAN_POINT ( 'NONE',  ( 106.4257688009193998, 0.000000000000000000, 289.4830310981789125 ) ) ;
#40058=( NAMED_UNIT ( * ) PLANE_ANGLE_UNIT ( ) SI_UNIT ( $, .RADIAN. ) );
#40079=DIRECTION ( 'NONE',  ( 0.000000000000000000, 0.000000000000000000, 1.000000000000000000 ) ) ;
#40216=EDGE_CURVE ( 'NONE', #31017, #61884, #54265, .T. ) ;
#40233=ORIENTED_EDGE ( 'NONE', *, *, #6803, .T. ) ;
#40234=PRODUCT_DEFINITION_CONTEXT ( 'detailed design', #38180, 'design' ) ;
#40306=EDGE_CURVE ( 'NONE', #48443, #18655, #52210, .T. ) ;
#40412=AXIS2_PLACEMENT_3D ( 'NONE', #51982, #36780, #8841 ) ;
#40431=EDGE_CURVE ( 'NONE', #527, #46607, #16483, .T. ) ;
#40593=ORIENTED_EDGE ( 'NONE', *, *, #44228, .F. ) ;
#40800=CARTESIAN_POINT ( 'NONE',  ( 75.42576880091937142, 0.000000000000000000, 289.4830310981789125 ) ) ;
#41358=ORIENTED_EDGE ( 'NONE', *, *, #40431, .F. ) ;
#41429=FACE_BOUND ( 'NONE', #33395, .T. ) ;
#41461=CARTESIAN_POINT ( 'NONE',  ( 75.42576880091934299, 10.00000000000000000, 330.9830310981789694 ) ) ;
#41473=DIRECTION ( 'NONE',  ( 0.000000000000000000, 0.000000000000000000, 1.000000000000000000 ) ) ;
#41542=LINE ( 'NONE', #37292, #19866 ) ;
#41620=CARTESIAN_POINT ( 'NONE',  ( 106.4257688009193998, 0.000000000000000000, 282.4830310981789125 ) ) ;
#41645=EDGE_CURVE ( 'NONE', #46607, #20190, #57448, .T. ) ;
#41664=ORIENTED_EDGE ( 'NONE', *, *, #45773, .T. ) ;
#41690=VECTOR ( 'NONE', #66704, 1000.000000000000000 ) ;
#41694=EDGE_CURVE ( 'NONE', #61884, #31017, #31654, .T. ) ;
#41786=SURFACE_STYLE_FILL_AREA ( #36484 ) ;
#42049=CARTESIAN_POINT ( 'NONE',  ( 106.4257688009193430, 10.00000000000000000, 330.9830310981789694 ) ) ;
#42076=ADVANCED_FACE ( 'NONE', ( #4306 ), #3941, .F. ) ;
#42151=AXIS2_PLACEMENT_3D ( 'NONE', #53621, #5871, #58578 ) ;
#42257=AXIS2_PLACEMENT_3D ( 'NONE', #61391, #3077, #51509 ) ;
#42299=DIRECTION ( 'NONE',  ( 0.000000000000000000, 0.000000000000000000, 1.000000000000000000 ) ) ;
#42466=EDGE_LOOP ( 'NONE', ( #27232, #31429, #63887, #20175 ) ) ;
#42789=EDGE_CURVE ( 'NONE', #23385, #19716, #11319, .T. ) ;
#42826=VERTEX_POINT ( 'NONE', #50543 ) ;
#42933=ADVANCED_FACE ( 'NONE', ( #3504 ), #57590, .F. ) ;
#43096=CLOSED_SHELL ( 'NONE', ( #42933, #23305, #61608, #67790, #23916, #2328, #10777, #52559, #20323, #27843, #42076, #14263, #10091, #64764 ) ) ;
#43329=CARTESIAN_POINT ( 'NONE',  ( 69.92576880110416937, 10.00000000000000000, 335.4830310981152479 ) ) ;
#43555=DIRECTION ( 'NONE',  ( 0.000000000000000000, 0.000000000000000000, 1.000000000000000000 ) ) ;
#43630=EDGE_CURVE ( 'NONE', #65210, #33597, #28862, .T. ) ;
#43671=ORIENTED_EDGE ( 'NONE', *, *, #41645, .T. ) ;
#44228=EDGE_CURVE ( 'NONE', #31017, #66383, #57168, .T. ) ;
#44286=AXIS2_PLACEMENT_3D ( 'NONE', #7101, #28679, #18064 ) ;
#44291=EDGE_LOOP ( 'NONE', ( #4665, #34998, #17025, #12843 ) ) ;
#44562=AXIS2_PLACEMENT_3D ( 'NONE', #67911, #62589, #68963 ) ;
#45124=CARTESIAN_POINT ( 'NONE',  ( 69.92576880110368620, 10.00000000000000000, 281.4830310981151911 ) ) ;
#45188=CARTESIAN_POINT ( 'NONE',  ( 75.42576880091934299, 10.00000000000000000, 334.4830310981790831 ) ) ;
#45326=EDGE_CURVE ( 'NONE', #9530, #48443, #23268, .T. ) ;
#45511=DIRECTION ( 'NONE',  ( 0.000000000000000000, 0.000000000000000000, 1.000000000000000000 ) ) ;
#45773=EDGE_CURVE ( 'NONE', #18655, #27811, #57239, .T. ) ;
#45902=EDGE_LOOP ( 'NONE', ( #40233, #11278 ) ) ;
#45918=AXIS2_PLACEMENT_3D ( 'NONE', #22775, #53934, #32355 ) ;
#45934=CARTESIAN_POINT ( 'NONE',  ( 106.4257688009193430, 0.000000000000000000, 330.9830310981789694 ) ) ;
#45960=EDGE_LOOP ( 'NONE', ( #38143, #22042, #56410, #69347 ) ) ;
#46137=CARTESIAN_POINT ( 'NONE',  ( 75.42576880091937142, 0.000000000000000000, 285.9830310981789125 ) ) ;
#46175=EDGE_CURVE ( 'NONE', #65210, #68276, #36739, .T. ) ;
#46495=DIRECTION ( 'NONE',  ( 0.000000000000000000, 0.000000000000000000, 1.000000000000000000 ) ) ;
#46607=VERTEX_POINT ( 'NONE', #30642 ) ;
#46939=ORIENTED_EDGE ( 'NONE', *, *, #13728, .F. ) ;
#47472=CARTESIAN_POINT ( 'NONE',  ( 75.42576880091934299, 10.00000000000000000, 330.9830310981789694 ) ) ;
#47499=ORIENTED_EDGE ( 'NONE', *, *, #44228, .T. ) ;
#47609=DIRECTION ( 'NONE',  ( 0.000000000000000000, 0.000000000000000000, 1.000000000000000000 ) ) ;
#47782=PLANE ( 'NONE',  #1891 ) ;
#48081=ORIENTED_EDGE ( 'NONE', *, *, #34281, .F. ) ;
#48152=FILL_AREA_STYLE_COLOUR ( '', #21242 ) ;
#48247=CIRCLE ( 'NONE', #17748, 3.500000000000003109 ) ;
#48337=STYLED_ITEM ( 'NONE', ( #58056 ), #21303 ) ;
#48443=VERTEX_POINT ( 'NONE', #48935 ) ;
#48796=ORIENTED_EDGE ( 'NONE', *, *, #41645, .F. ) ;
#48840=ORIENTED_EDGE ( 'NONE', *, *, #9540, .T. ) ;
#48875=CYLINDRICAL_SURFACE ( 'NONE', #54877, 3.500000000000003109 ) ;
#48935=CARTESIAN_POINT ( 'NONE',  ( 106.4257688009193430, 0.000000000000000000, 334.4830310981789694 ) ) ;
#49303=CARTESIAN_POINT ( 'NONE',  ( 111.9257688011041836, 10.00000000000000000, 281.4830310981151911 ) ) ;
#49315=EDGE_LOOP ( 'NONE', ( #9409, #14425 ) ) ;
#49425=EDGE_LOOP ( 'NONE', ( #46939, #48796, #63446, #62009 ) ) ;
#49776=SHAPE_REPRESENTATION ( 'Part1', ( #45918 ), #66261 ) ;
#49914=VECTOR ( 'NONE', #59446, 1000.000000000000000 ) ;
#50066=AXIS2_PLACEMENT_3D ( 'NONE', #68828, #20385, #4483 ) ;
#50310=DIRECTION ( 'NONE',  ( -0.000000000000000000, 1.000000000000000000, -0.000000000000000000 ) ) ;
#50537=FACE_BOUND ( 'NONE', #45902, .T. ) ;
#50543=CARTESIAN_POINT ( 'NONE',  ( 106.4257688009193998, 10.00000000000000000, 282.4830310981789125 ) ) ;
#50624=CARTESIAN_POINT ( 'NONE',  ( 111.9257688011037146, 10.00000000000000000, 335.4830310981152479 ) ) ;
#50931=CIRCLE ( 'NONE', #69018, 3.500000000000003109 ) ;
#50991=ORIENTED_EDGE ( 'NONE', *, *, #9540, .F. ) ;
#51122=ORIENTED_EDGE ( 'NONE', *, *, #55375, .F. ) ;
#51382=SHAPE_REPRESENTATION_RELATIONSHIP ( 'NONE' , 'NONE' ,  #49776, #8117 ) ;
#51509=DIRECTION ( 'NONE',  ( -8.480870326997715333E-15, 0.000000000000000000, 1.000000000000000000 ) ) ;
#51536=DIRECTION ( 'NONE',  ( -0.000000000000000000, 1.000000000000000000, -0.000000000000000000 ) ) ;
#51885=LINE ( 'NONE', #41620, #65985 ) ;
#51982=CARTESIAN_POINT ( 'NONE',  ( 69.92576880110368620, 10.00000000000000000, 281.4830310981151911 ) ) ;
#52019=ORIENTED_EDGE ( 'NONE', *, *, #18728, .T. ) ;
#52210=LINE ( 'NONE', #10133, #29399 ) ;
#52559=ADVANCED_FACE ( 'NONE', ( #68707 ), #10349, .F. ) ;
#52751=DIRECTION ( 'NONE',  ( 0.000000000000000000, 0.000000000000000000, 1.000000000000000000 ) ) ;
#52972=DIRECTION ( 'NONE',  ( 1.000000000000000000, 0.000000000000000000, 0.000000000000000000 ) ) ;
#52974=EDGE_CURVE ( 'NONE', #33597, #65210, #35533, .T. ) ;
#53049=ORIENTED_EDGE ( 'NONE', *, *, #39745, .F. ) ;
#53079=VECTOR ( 'NONE', #14783, 1000.000000000000000 ) ;
#53278=EDGE_CURVE ( 'NONE', #61884, #33102, #31043, .T. ) ;
#53621=CARTESIAN_POINT ( 'NONE',  ( 75.42576880091937142, 10.00000000000000000, 285.9830310981789125 ) ) ;
#53660=CARTESIAN_POINT ( 'NONE',  ( 69.92576880110416937, 0.000000000000000000, 335.4830310981152479 ) ) ;
#53704=DIRECTION ( 'NONE',  ( 0.000000000000000000, 1.000000000000000000, 0.000000000000000000 ) ) ;
#53934=DIRECTION ( 'NONE',  ( 0.000000000000000000, 0.000000000000000000, 1.000000000000000000 ) ) ;
#54265=CIRCLE ( 'NONE', #21494, 3.500000000000003109 ) ;
#54562=VECTOR ( 'NONE', #12660, 1000.000000000000000 ) ;
#54735=CARTESIAN_POINT ( 'NONE',  ( 106.4257688009193430, 0.000000000000000000, 327.4830310981789694 ) ) ;
#54807=FACE_BOUND ( 'NONE', #37219, .T. ) ;
#54877=AXIS2_PLACEMENT_3D ( 'NONE', #22685, #1126, #43555 ) ;
#54947=DIRECTION ( 'NONE',  ( 0.000000000000000000, 0.000000000000000000, 1.000000000000000000 ) ) ;
#55018=CARTESIAN_POINT ( 'NONE',  ( 111.9257688011041836, 10.00000000000000000, 281.4830310981151911 ) ) ;
#55079=VECTOR ( 'NONE', #52972, 1000.000000000000000 ) ;
#55210=CARTESIAN_POINT ( 'NONE',  ( 75.42576880091937142, 10.00000000000000000, 289.4830310981789125 ) ) ;
#55375=EDGE_CURVE ( 'NONE', #527, #23385, #57693, .T. ) ;
#55497=EDGE_CURVE ( 'NONE', #22621, #46607, #11340, .T. ) ;
#55831=CARTESIAN_POINT ( 'NONE',  ( 75.42576880091937142, 0.000000000000000000, 285.9830310981789125 ) ) ;
#56254=FACE_OUTER_BOUND ( 'NONE', #15940, .T. ) ;
#56376=ORIENTED_EDGE ( 'NONE', *, *, #4333, .F. ) ;
#56395=CARTESIAN_POINT ( 'NONE',  ( 69.92576880110368620, 0.000000000000000000, 281.4830310981151911 ) ) ;
#56410=ORIENTED_EDGE ( 'NONE', *, *, #4333, .T. ) ;
#57168=LINE ( 'NONE', #58220, #37827 ) ;
#57239=CIRCLE ( 'NONE', #23317, 3.500000000000003109 ) ;
#57404=VERTEX_POINT ( 'NONE', #29959 ) ;
#57448=LINE ( 'NONE', #56395, #22651 ) ;
#57566=PRODUCT_CONTEXT ( 'NONE', #17819, 'mechanical' ) ;
#57590=CYLINDRICAL_SURFACE ( 'NONE', #28611, 3.500000000000003109 ) ;
#57693=LINE ( 'NONE', #9264, #26209 ) ;
#57721=CARTESIAN_POINT ( 'NONE',  ( 69.92576880110416937, 0.000000000000000000, 335.4830310981152479 ) ) ;
#58056=PRESENTATION_STYLE_ASSIGNMENT (( #64086 ) ) ;
#58220=CARTESIAN_POINT ( 'NONE',  ( 75.42576880091937142, 0.000000000000000000, 282.4830310981789125 ) ) ;
#58415=FACE_OUTER_BOUND ( 'NONE', #24169, .T. ) ;
#58578=DIRECTION ( 'NONE',  ( 0.000000000000000000, 0.000000000000000000, 1.000000000000000000 ) ) ;
#58612=EDGE_LOOP ( 'NONE', ( #43671, #50991, #51122, #17002 ) ) ;
#58910=CIRCLE ( 'NONE', #65666, 3.500000000000114131 ) ;
#59432=CYLINDRICAL_SURFACE ( 'NONE', #38172, 3.500000000000114131 ) ;
#59446=DIRECTION ( 'NONE',  ( 8.480870326997715333E-15, -0.000000000000000000, -1.000000000000000000 ) ) ;
#60084=AXIS2_PLACEMENT_3D ( 'NONE', #33132, #33483, #22536 ) ;
#60430=CYLINDRICAL_SURFACE ( 'NONE', #61754, 3.500000000000003109 ) ;
#60611=ORIENTED_EDGE ( 'NONE', *, *, #64810, .T. ) ;
#60789=CARTESIAN_POINT ( 'NONE',  ( 0.000000000000000000, 0.000000000000000000, 0.000000000000000000 ) ) ;
#61391=CARTESIAN_POINT ( 'NONE',  ( 111.9257688011041836, 10.00000000000000000, 281.4830310981151911 ) ) ;
#61608=ADVANCED_FACE ( 'NONE', ( #13390 ), #60430, .F. ) ;
#61754=AXIS2_PLACEMENT_3D ( 'NONE', #55831, #1062, #7034 ) ;
#61884=VERTEX_POINT ( 'NONE', #40800 ) ;
#62009=ORIENTED_EDGE ( 'NONE', *, *, #69564, .F. ) ;
#62249=EDGE_LOOP ( 'NONE', ( #69465, #39187, #67739, #48840 ) ) ;
#62405=VERTEX_POINT ( 'NONE', #50624 ) ;
#62568=FACE_OUTER_BOUND ( 'NONE', #62249, .T. ) ;
#62589=DIRECTION ( 'NONE',  ( 0.000000000000000000, 1.000000000000000000, 0.000000000000000000 ) ) ;
#62833=ORIENTED_EDGE ( 'NONE', *, *, #6803, .F. ) ;
#62913=LINE ( 'NONE', #36033, #37259 ) ;
#63446=ORIENTED_EDGE ( 'NONE', *, *, #55497, .F. ) ;
#63517=CARTESIAN_POINT ( 'NONE',  ( 75.42576880091937142, 10.00000000000000000, 285.9830310981789125 ) ) ;
#63887=ORIENTED_EDGE ( 'NONE', *, *, #46175, .T. ) ;
#64043=ORIENTED_EDGE ( 'NONE', *, *, #39745, .T. ) ;
#64070=CARTESIAN_POINT ( 'NONE',  ( 69.92576880110416937, 10.00000000000000000, 335.4830310981152479 ) ) ;
#64086=SURFACE_STYLE_USAGE ( .BOTH. , #36130 ) ;
#64512=DIRECTION ( 'NONE',  ( -0.000000000000000000, -1.000000000000000000, -0.000000000000000000 ) ) ;
#64742=LINE ( 'NONE', #64070, #29289 ) ;
#64764=ADVANCED_FACE ( 'NONE', ( #9426 ), #30995, .F. ) ;
#64810=EDGE_CURVE ( 'NONE', #66383, #33102, #16164, .T. ) ;
#64896=UNCERTAINTY_MEASURE_WITH_UNIT (LENGTH_MEASURE( 1.000000000000000082E-05 ), #18157, 'distance_accuracy_value', 'NONE');
#65082=AXIS2_PLACEMENT_3D ( 'NONE', #29139, #24547, #40079 ) ;
#65210=VERTEX_POINT ( 'NONE', #7469 ) ;
#65421=CARTESIAN_POINT ( 'NONE',  ( 106.4257688009193430, 10.00000000000000000, 327.4830310981789694 ) ) ;
#65666=AXIS2_PLACEMENT_3D ( 'NONE', #41461, #20239, #14944 ) ;
#65985=VECTOR ( 'NONE', #51536, 1000.000000000000000 ) ;
#66071=CARTESIAN_POINT ( 'NONE',  ( 69.92576880110416937, 10.00000000000000000, 335.4830310981152479 ) ) ;
#66091=FACE_BOUND ( 'NONE', #32542, .T. ) ;
#66177=ORIENTED_EDGE ( 'NONE', *, *, #45773, .F. ) ;
#66198=CIRCLE ( 'NONE', #36900, 3.500000000000003109 ) ;
#66261=( GEOMETRIC_REPRESENTATION_CONTEXT ( 3 ) GLOBAL_UNCERTAINTY_ASSIGNED_CONTEXT ( ( #64896 ) ) GLOBAL_UNIT_ASSIGNED_CONTEXT ( ( #18157, #40058, #35108 ) ) REPRESENTATION_CONTEXT ( 'NONE', 'WORKASPACE' ) );
#66383=VERTEX_POINT ( 'NONE', #16419 ) ;
#66439=ORIENTED_EDGE ( 'NONE', *, *, #67554, .T. ) ;
#66704=DIRECTION ( 'NONE',  ( -0.000000000000000000, -1.000000000000000000, -0.000000000000000000 ) ) ;
#66783=FACE_BOUND ( 'NONE', #49315, .T. ) ;
#66815=LINE ( 'NONE', #28301, #35716 ) ;
#67077=AXIS2_PLACEMENT_3D ( 'NONE', #5039, #41473, #14954 ) ;
#67431=FACE_OUTER_BOUND ( 'NONE', #11535, .T. ) ;
#67514=DIRECTION ( 'NONE',  ( 0.000000000000000000, 0.000000000000000000, 1.000000000000000000 ) ) ;
#67554=EDGE_CURVE ( 'NONE', #27638, #57404, #3287, .T. ) ;
#67739=ORIENTED_EDGE ( 'NONE', *, *, #42789, .F. ) ;
#67740=ORIENTED_EDGE ( 'NONE', *, *, #53278, .F. ) ;
#67745=CARTESIAN_POINT ( 'NONE',  ( 106.4257688009193998, 0.000000000000000000, 285.9830310981789125 ) ) ;
#67790=ADVANCED_FACE ( 'NONE', ( #6757 ), #48875, .F. ) ;
#67911=CARTESIAN_POINT ( 'NONE',  ( 75.42576880091934299, 0.000000000000000000, 330.9830310981789694 ) ) ;
#68276=VERTEX_POINT ( 'NONE', #45188 ) ;
#68707=FACE_OUTER_BOUND ( 'NONE', #58612, .T. ) ;
#68828=CARTESIAN_POINT ( 'NONE',  ( 106.4257688009193430, 0.000000000000000000, 330.9830310981789694 ) ) ;
#68963=DIRECTION ( 'NONE',  ( 0.000000000000000000, 0.000000000000000000, 1.000000000000000000 ) ) ;
#69000=CARTESIAN_POINT ( 'NONE',  ( 75.42576880091934299, 0.000000000000000000, 330.9830310981789694 ) ) ;
#69018=AXIS2_PLACEMENT_3D ( 'NONE', #67745, #18602, #34858 ) ;
#69040=DIRECTION ( 'NONE',  ( 0.000000000000000000, 0.000000000000000000, 1.000000000000000000 ) ) ;
#69071=EDGE_LOOP ( 'NONE', ( #33502, #22340, #4687, #38630 ) ) ;
#69213=EDGE_CURVE ( 'NONE', #33597, #10103, #39202, .T. ) ;
#69347=ORIENTED_EDGE ( 'NONE', *, *, #46175, .F. ) ;
#69465=ORIENTED_EDGE ( 'NONE', *, *, #13728, .T. ) ;
#69564=EDGE_CURVE ( 'NONE', #24845, #22621, #32086, .T. ) ;
#69693=CARTESIAN_POINT ( 'NONE',  ( 106.4257688009193998, 0.000000000000000000, 282.4830310981789125 ) ) ;
#69733=EDGE_LOOP ( 'NONE', ( #31108, #13949, #10431, #41664 ) ) ;
ENDSEC;
END-ISO-10303-21;
